ISO-10303-21;
HEADER;
/* Generated by software containing ST-Developer
 * from STEP Tools, Inc. (www.steptools.com) 
 */

FILE_DESCRIPTION(
/* description */ ('Counterbalanced vertical column'),
/* implementation_level */ '2;1');

FILE_NAME(
/* name */ 'M5x30 frame screw.step',
/* time_stamp */ '2026-10-29T16:47:22-07:00',
/* author */ (''),
/* organization */ (''),
/* preprocessor_version */ 'ST-DEVELOPER v20.2',
/* originating_system */ 'Autodesk Translation Framework v15.17.0.0',
/* authorisation */ '');

FILE_SCHEMA (('AUTOMOTIVE_DESIGN { 1 0 10303 214 3 1 1 }'));
ENDSEC;

DATA;
#10=MECHANICAL_DESIGN_GEOMETRIC_PRESENTATION_REPRESENTATION('',(#369),#15040);
#247=CONICAL_SURFACE('',#7862,0.4,0.785398163397448);
#248=CONICAL_SURFACE('',#7866,0.41,0.785398163397448);
#249=CONICAL_SURFACE('',#7870,0.26,0.463647609000806);
#262=ORIENTED_CLOSED_SHELL('',*,#7092,.F.);
#266=BREP_WITH_VOIDS('Body1',#7093,(#262));
#299=SHAPE_REPRESENTATION_RELATIONSHIP('SRR','None',#15203,#334);
#334=ADVANCED_BREP_SHAPE_REPRESENTATION('',(#266),#15022);
#369=STYLED_ITEM('',(#15464),#266);
#492=FACE_BOUND('',#1525,.T.);
#493=FACE_BOUND('',#1533,.T.);
#683=PLANE('',#7846);
#684=PLANE('',#7847);
#685=PLANE('',#7848);
#686=PLANE('',#7849);
#687=PLANE('',#7850);
#688=PLANE('',#7851);
#689=PLANE('',#7852);
#690=PLANE('',#7853);
#691=PLANE('',#7854);
#692=PLANE('',#7859);
#693=PLANE('',#7860);
#694=PLANE('',#7868);
#1035=FACE_OUTER_BOUND('',#1516,.T.);
#1036=FACE_OUTER_BOUND('',#1517,.T.);
#1037=FACE_OUTER_BOUND('',#1518,.T.);
#1038=FACE_OUTER_BOUND('',#1519,.T.);
#1039=FACE_OUTER_BOUND('',#1520,.T.);
#1040=FACE_OUTER_BOUND('',#1521,.T.);
#1041=FACE_OUTER_BOUND('',#1522,.T.);
#1042=FACE_OUTER_BOUND('',#1523,.T.);
#1043=FACE_OUTER_BOUND('',#1524,.T.);
#1044=FACE_OUTER_BOUND('',#1526,.T.);
#1045=FACE_OUTER_BOUND('',#1527,.T.);
#1046=FACE_OUTER_BOUND('',#1528,.T.);
#1047=FACE_OUTER_BOUND('',#1529,.T.);
#1048=FACE_OUTER_BOUND('',#1530,.T.);
#1049=FACE_OUTER_BOUND('',#1531,.T.);
#1050=FACE_OUTER_BOUND('',#1532,.T.);
#1051=FACE_OUTER_BOUND('',#1534,.T.);
#1052=FACE_OUTER_BOUND('',#1535,.T.);
#1516=EDGE_LOOP('',(#5706,#5707,#5708,#5709));
#1517=EDGE_LOOP('',(#5710,#5711,#5712,#5713));
#1518=EDGE_LOOP('',(#5714,#5715,#5716,#5717));
#1519=EDGE_LOOP('',(#5718,#5719,#5720,#5721));
#1520=EDGE_LOOP('',(#5722,#5723,#5724,#5725));
#1521=EDGE_LOOP('',(#5726,#5727,#5728,#5729));
#1522=EDGE_LOOP('',(#5730,#5731,#5732,#5733,#5734,#5735));
#1523=EDGE_LOOP('',(#5736,#5737,#5738,#5739,#5740,#5741));
#1524=EDGE_LOOP('',(#5742));
#1525=EDGE_LOOP('',(#5743));
#1526=EDGE_LOOP('',(#5744,#5745,#5746,#5747));
#1527=EDGE_LOOP('',(#5748));
#1528=EDGE_LOOP('',(#5749));
#1529=EDGE_LOOP('',(#5750,#5751,#5752,#5753));
#1530=EDGE_LOOP('',(#5754,#5755,#5756,#5757));
#1531=EDGE_LOOP('',(#5758,#5759,#5760,#5761));
#1532=EDGE_LOOP('',(#5762));
#1533=EDGE_LOOP('',(#5763));
#1534=EDGE_LOOP('',(#5764,#5765,#5766,#5767));
#1535=EDGE_LOOP('',(#5768,#5769,#5770,#5771));
#2091=LINE('',#13975,#2762);
#2092=LINE('',#13977,#2763);
#2093=LINE('',#13979,#2764);
#2094=LINE('',#13980,#2765);
#2095=LINE('',#13983,#2766);
#2096=LINE('',#13985,#2767);
#2097=LINE('',#13986,#2768);
#2098=LINE('',#13989,#2769);
#2099=LINE('',#13991,#2770);
#2100=LINE('',#13992,#2771);
#2101=LINE('',#13995,#2772);
#2102=LINE('',#13997,#2773);
#2103=LINE('',#13998,#2774);
#2104=LINE('',#14001,#2775);
#2105=LINE('',#14003,#2776);
#2106=LINE('',#14004,#2777);
#2107=LINE('',#14006,#2778);
#2108=LINE('',#14007,#2779);
#2109=LINE('',#14017,#2780);
#2110=LINE('',#14026,#2781);
#2111=LINE('',#14030,#2782);
#2112=LINE('',#14034,#2783);
#2113=LINE('',#14041,#2784);
#2114=LINE('',#14043,#2785);
#2762=VECTOR('',#9259,1.);
#2763=VECTOR('',#9260,1.);
#2764=VECTOR('',#9261,1.);
#2765=VECTOR('',#9262,1.);
#2766=VECTOR('',#9265,1.);
#2767=VECTOR('',#9266,1.);
#2768=VECTOR('',#9267,1.);
#2769=VECTOR('',#9270,1.);
#2770=VECTOR('',#9271,1.);
#2771=VECTOR('',#9272,1.);
#2772=VECTOR('',#9275,1.);
#2773=VECTOR('',#9276,1.);
#2774=VECTOR('',#9277,1.);
#2775=VECTOR('',#9280,1.);
#2776=VECTOR('',#9281,1.);
#2777=VECTOR('',#9282,1.);
#2778=VECTOR('',#9285,1.);
#2779=VECTOR('',#9286,1.);
#2780=VECTOR('',#9299,0.25);
#2781=VECTOR('',#9312,0.4);
#2782=VECTOR('',#9317,0.425);
#2783=VECTOR('',#9322,0.41);
#2784=VECTOR('',#9331,0.26);
#2785=VECTOR('',#9334,0.25);
#3205=CIRCLE('',#7855,0.25);
#3206=CIRCLE('',#7856,0.24505);
#3207=CIRCLE('',#7858,0.25);
#3208=CIRCLE('',#7861,0.375);
#3209=CIRCLE('',#7863,0.425);
#3210=CIRCLE('',#7865,0.425);
#3211=CIRCLE('',#7867,0.395);
#3212=CIRCLE('',#7869,0.27);
#3213=CIRCLE('',#7871,0.24505);
#3612=VERTEX_POINT('',#13973);
#3613=VERTEX_POINT('',#13974);
#3614=VERTEX_POINT('',#13976);
#3615=VERTEX_POINT('',#13978);
#3616=VERTEX_POINT('',#13982);
#3617=VERTEX_POINT('',#13984);
#3618=VERTEX_POINT('',#13988);
#3619=VERTEX_POINT('',#13990);
#3620=VERTEX_POINT('',#13994);
#3621=VERTEX_POINT('',#13996);
#3622=VERTEX_POINT('',#14000);
#3623=VERTEX_POINT('',#14002);
#3624=VERTEX_POINT('',#14011);
#3625=VERTEX_POINT('',#14013);
#3626=VERTEX_POINT('',#14016);
#3627=VERTEX_POINT('',#14021);
#3628=VERTEX_POINT('',#14024);
#3629=VERTEX_POINT('',#14028);
#3630=VERTEX_POINT('',#14032);
#3631=VERTEX_POINT('',#14036);
#3632=VERTEX_POINT('',#14039);
#4354=EDGE_CURVE('',#3612,#3613,#2091,.T.);
#4355=EDGE_CURVE('',#3613,#3614,#2092,.T.);
#4356=EDGE_CURVE('',#3614,#3615,#2093,.T.);
#4357=EDGE_CURVE('',#3612,#3615,#2094,.T.);
#4358=EDGE_CURVE('',#3613,#3616,#2095,.T.);
#4359=EDGE_CURVE('',#3616,#3617,#2096,.T.);
#4360=EDGE_CURVE('',#3617,#3614,#2097,.T.);
#4361=EDGE_CURVE('',#3616,#3618,#2098,.T.);
#4362=EDGE_CURVE('',#3618,#3619,#2099,.T.);
#4363=EDGE_CURVE('',#3619,#3617,#2100,.T.);
#4364=EDGE_CURVE('',#3618,#3620,#2101,.T.);
#4365=EDGE_CURVE('',#3620,#3621,#2102,.T.);
#4366=EDGE_CURVE('',#3621,#3619,#2103,.T.);
#4367=EDGE_CURVE('',#3620,#3622,#2104,.T.);
#4368=EDGE_CURVE('',#3622,#3623,#2105,.T.);
#4369=EDGE_CURVE('',#3623,#3621,#2106,.T.);
#4370=EDGE_CURVE('',#3622,#3612,#2107,.T.);
#4371=EDGE_CURVE('',#3615,#3623,#2108,.T.);
#4372=EDGE_CURVE('',#3624,#3624,#3205,.T.);
#4373=EDGE_CURVE('',#3625,#3625,#3206,.T.);
#4374=EDGE_CURVE('',#3624,#3626,#2109,.T.);
#4375=EDGE_CURVE('',#3626,#3626,#3207,.T.);
#4376=EDGE_CURVE('',#3627,#3627,#3208,.T.);
#4377=EDGE_CURVE('',#3628,#3628,#3209,.T.);
#4378=EDGE_CURVE('',#3628,#3627,#2110,.T.);
#4379=EDGE_CURVE('',#3629,#3629,#3210,.T.);
#4380=EDGE_CURVE('',#3629,#3628,#2111,.T.);
#4381=EDGE_CURVE('',#3630,#3630,#3211,.T.);
#4382=EDGE_CURVE('',#3630,#3629,#2112,.T.);
#4383=EDGE_CURVE('',#3631,#3631,#3212,.T.);
#4384=EDGE_CURVE('',#3632,#3632,#3213,.F.);
#4385=EDGE_CURVE('',#3632,#3631,#2113,.T.);
#4386=EDGE_CURVE('',#3625,#3632,#2114,.T.);
#5706=ORIENTED_EDGE('',*,*,#4354,.T.);
#5707=ORIENTED_EDGE('',*,*,#4355,.T.);
#5708=ORIENTED_EDGE('',*,*,#4356,.T.);
#5709=ORIENTED_EDGE('',*,*,#4357,.F.);
#5710=ORIENTED_EDGE('',*,*,#4358,.T.);
#5711=ORIENTED_EDGE('',*,*,#4359,.T.);
#5712=ORIENTED_EDGE('',*,*,#4360,.T.);
#5713=ORIENTED_EDGE('',*,*,#4355,.F.);
#5714=ORIENTED_EDGE('',*,*,#4361,.T.);
#5715=ORIENTED_EDGE('',*,*,#4362,.T.);
#5716=ORIENTED_EDGE('',*,*,#4363,.T.);
#5717=ORIENTED_EDGE('',*,*,#4359,.F.);
#5718=ORIENTED_EDGE('',*,*,#4364,.T.);
#5719=ORIENTED_EDGE('',*,*,#4365,.T.);
#5720=ORIENTED_EDGE('',*,*,#4366,.T.);
#5721=ORIENTED_EDGE('',*,*,#4362,.F.);
#5722=ORIENTED_EDGE('',*,*,#4367,.T.);
#5723=ORIENTED_EDGE('',*,*,#4368,.T.);
#5724=ORIENTED_EDGE('',*,*,#4369,.T.);
#5725=ORIENTED_EDGE('',*,*,#4365,.F.);
#5726=ORIENTED_EDGE('',*,*,#4370,.T.);
#5727=ORIENTED_EDGE('',*,*,#4357,.T.);
#5728=ORIENTED_EDGE('',*,*,#4371,.T.);
#5729=ORIENTED_EDGE('',*,*,#4368,.F.);
#5730=ORIENTED_EDGE('',*,*,#4370,.F.);
#5731=ORIENTED_EDGE('',*,*,#4367,.F.);
#5732=ORIENTED_EDGE('',*,*,#4364,.F.);
#5733=ORIENTED_EDGE('',*,*,#4361,.F.);
#5734=ORIENTED_EDGE('',*,*,#4358,.F.);
#5735=ORIENTED_EDGE('',*,*,#4354,.F.);
#5736=ORIENTED_EDGE('',*,*,#4371,.F.);
#5737=ORIENTED_EDGE('',*,*,#4356,.F.);
#5738=ORIENTED_EDGE('',*,*,#4360,.F.);
#5739=ORIENTED_EDGE('',*,*,#4363,.F.);
#5740=ORIENTED_EDGE('',*,*,#4366,.F.);
#5741=ORIENTED_EDGE('',*,*,#4369,.F.);
#5742=ORIENTED_EDGE('',*,*,#4372,.T.);
#5743=ORIENTED_EDGE('',*,*,#4373,.F.);
#5744=ORIENTED_EDGE('',*,*,#4372,.F.);
#5745=ORIENTED_EDGE('',*,*,#4374,.T.);
#5746=ORIENTED_EDGE('',*,*,#4375,.T.);
#5747=ORIENTED_EDGE('',*,*,#4374,.F.);
#5748=ORIENTED_EDGE('',*,*,#4375,.F.);
#5749=ORIENTED_EDGE('',*,*,#4376,.F.);
#5750=ORIENTED_EDGE('',*,*,#4377,.F.);
#5751=ORIENTED_EDGE('',*,*,#4378,.T.);
#5752=ORIENTED_EDGE('',*,*,#4376,.T.);
#5753=ORIENTED_EDGE('',*,*,#4378,.F.);
#5754=ORIENTED_EDGE('',*,*,#4379,.F.);
#5755=ORIENTED_EDGE('',*,*,#4380,.T.);
#5756=ORIENTED_EDGE('',*,*,#4377,.T.);
#5757=ORIENTED_EDGE('',*,*,#4380,.F.);
#5758=ORIENTED_EDGE('',*,*,#4381,.F.);
#5759=ORIENTED_EDGE('',*,*,#4382,.T.);
#5760=ORIENTED_EDGE('',*,*,#4379,.T.);
#5761=ORIENTED_EDGE('',*,*,#4382,.F.);
#5762=ORIENTED_EDGE('',*,*,#4381,.T.);
#5763=ORIENTED_EDGE('',*,*,#4383,.F.);
#5764=ORIENTED_EDGE('',*,*,#4384,.F.);
#5765=ORIENTED_EDGE('',*,*,#4385,.T.);
#5766=ORIENTED_EDGE('',*,*,#4383,.T.);
#5767=ORIENTED_EDGE('',*,*,#4385,.F.);
#5768=ORIENTED_EDGE('',*,*,#4373,.T.);
#5769=ORIENTED_EDGE('',*,*,#4386,.T.);
#5770=ORIENTED_EDGE('',*,*,#4384,.T.);
#5771=ORIENTED_EDGE('',*,*,#4386,.F.);
#6630=CYLINDRICAL_SURFACE('',#7857,0.25);
#6631=CYLINDRICAL_SURFACE('',#7864,0.425);
#6632=CYLINDRICAL_SURFACE('',#7872,0.24505);
#6877=ADVANCED_FACE('',(#1035),#683,.F.);
#6878=ADVANCED_FACE('',(#1036),#684,.F.);
#6879=ADVANCED_FACE('',(#1037),#685,.F.);
#6880=ADVANCED_FACE('',(#1038),#686,.F.);
#6881=ADVANCED_FACE('',(#1039),#687,.F.);
#6882=ADVANCED_FACE('',(#1040),#688,.F.);
#6883=ADVANCED_FACE('',(#1041),#689,.F.);
#6884=ADVANCED_FACE('',(#1042),#690,.F.);
#6885=ADVANCED_FACE('',(#1043,#492),#691,.T.);
#6886=ADVANCED_FACE('',(#1044),#6630,.T.);
#6887=ADVANCED_FACE('',(#1045),#692,.F.);
#6888=ADVANCED_FACE('',(#1046),#693,.T.);
#6889=ADVANCED_FACE('',(#1047),#247,.T.);
#6890=ADVANCED_FACE('',(#1048),#6631,.T.);
#6891=ADVANCED_FACE('',(#1049),#248,.T.);
#6892=ADVANCED_FACE('',(#1050,#493),#694,.T.);
#6893=ADVANCED_FACE('',(#1051),#249,.T.);
#6894=ADVANCED_FACE('',(#1052),#6632,.T.);
#7092=CLOSED_SHELL('',(#6877,#6878,#6879,#6880,#6881,#6882,#6883,#6884));
#7093=CLOSED_SHELL('',(#6885,#6886,#6887,#6888,#6889,#6890,#6891,#6892,
#6893,#6894));
#7845=AXIS2_PLACEMENT_3D('',#13971,#9255,#9256);
#7846=AXIS2_PLACEMENT_3D('',#13972,#9257,#9258);
#7847=AXIS2_PLACEMENT_3D('',#13981,#9263,#9264);
#7848=AXIS2_PLACEMENT_3D('',#13987,#9268,#9269);
#7849=AXIS2_PLACEMENT_3D('',#13993,#9273,#9274);
#7850=AXIS2_PLACEMENT_3D('',#13999,#9278,#9279);
#7851=AXIS2_PLACEMENT_3D('',#14005,#9283,#9284);
#7852=AXIS2_PLACEMENT_3D('',#14008,#9287,#9288);
#7853=AXIS2_PLACEMENT_3D('',#14009,#9289,#9290);
#7854=AXIS2_PLACEMENT_3D('',#14010,#9291,#9292);
#7855=AXIS2_PLACEMENT_3D('',#14012,#9293,#9294);
#7856=AXIS2_PLACEMENT_3D('',#14014,#9295,#9296);
#7857=AXIS2_PLACEMENT_3D('',#14015,#9297,#9298);
#7858=AXIS2_PLACEMENT_3D('',#14018,#9300,#9301);
#7859=AXIS2_PLACEMENT_3D('',#14019,#9302,#9303);
#7860=AXIS2_PLACEMENT_3D('',#14020,#9304,#9305);
#7861=AXIS2_PLACEMENT_3D('',#14022,#9306,#9307);
#7862=AXIS2_PLACEMENT_3D('',#14023,#9308,#9309);
#7863=AXIS2_PLACEMENT_3D('',#14025,#9310,#9311);
#7864=AXIS2_PLACEMENT_3D('',#14027,#9313,#9314);
#7865=AXIS2_PLACEMENT_3D('',#14029,#9315,#9316);
#7866=AXIS2_PLACEMENT_3D('',#14031,#9318,#9319);
#7867=AXIS2_PLACEMENT_3D('',#14033,#9320,#9321);
#7868=AXIS2_PLACEMENT_3D('',#14035,#9323,#9324);
#7869=AXIS2_PLACEMENT_3D('',#14037,#9325,#9326);
#7870=AXIS2_PLACEMENT_3D('',#14038,#9327,#9328);
#7871=AXIS2_PLACEMENT_3D('',#14040,#9329,#9330);
#7872=AXIS2_PLACEMENT_3D('',#14042,#9332,#9333);
#9255=DIRECTION('axis',(0.,0.,1.));
#9256=DIRECTION('refdir',(1.,0.,0.));
#9257=DIRECTION('center_axis',(0.866025403784439,0.,-0.5));
#9258=DIRECTION('ref_axis',(0.5,0.,0.866025403784439));
#9259=DIRECTION('',(-0.5,0.,-0.866025403784439));
#9260=DIRECTION('',(0.,-1.,0.));
#9261=DIRECTION('',(0.5,0.,0.866025403784439));
#9262=DIRECTION('',(0.,-1.,0.));
#9263=DIRECTION('center_axis',(1.20185167898973E-16,0.,-1.));
#9264=DIRECTION('ref_axis',(1.,0.,1.20185167898973E-16));
#9265=DIRECTION('',(-1.,0.,-1.20185167898973E-16));
#9266=DIRECTION('',(0.,-1.,0.));
#9267=DIRECTION('',(1.,0.,1.20185167898973E-16));
#9268=DIRECTION('center_axis',(-0.866025403784439,0.,-0.5));
#9269=DIRECTION('ref_axis',(0.5,0.,-0.866025403784439));
#9270=DIRECTION('',(-0.5,0.,0.866025403784439));
#9271=DIRECTION('',(0.,-1.,0.));
#9272=DIRECTION('',(0.5,0.,-0.866025403784439));
#9273=DIRECTION('center_axis',(-0.866025403784439,0.,0.5));
#9274=DIRECTION('ref_axis',(-0.5,0.,-0.866025403784439));
#9275=DIRECTION('',(0.5,0.,0.866025403784439));
#9276=DIRECTION('',(0.,-1.,0.));
#9277=DIRECTION('',(-0.5,0.,-0.866025403784439));
#9278=DIRECTION('center_axis',(-2.40370335797945E-16,0.,1.));
#9279=DIRECTION('ref_axis',(-1.,0.,-2.40370335797945E-16));
#9280=DIRECTION('',(1.,0.,2.40370335797945E-16));
#9281=DIRECTION('',(0.,-1.,0.));
#9282=DIRECTION('',(-1.,0.,-2.40370335797945E-16));
#9283=DIRECTION('center_axis',(0.866025403784439,0.,0.5));
#9284=DIRECTION('ref_axis',(-0.5,0.,0.866025403784439));
#9285=DIRECTION('',(0.5,0.,-0.866025403784439));
#9286=DIRECTION('',(-0.5,0.,0.866025403784439));
#9287=DIRECTION('center_axis',(0.,1.,0.));
#9288=DIRECTION('ref_axis',(1.,0.,0.));
#9289=DIRECTION('center_axis',(0.,-1.,0.));
#9290=DIRECTION('ref_axis',(0.,0.,-1.));
#9291=DIRECTION('center_axis',(0.,1.,0.));
#9292=DIRECTION('ref_axis',(1.,0.,0.));
#9293=DIRECTION('center_axis',(0.,1.,0.));
#9294=DIRECTION('ref_axis',(1.,0.,0.));
#9295=DIRECTION('center_axis',(0.,1.,0.));
#9296=DIRECTION('ref_axis',(1.,0.,0.));
#9297=DIRECTION('center_axis',(0.,1.,0.));
#9298=DIRECTION('ref_axis',(1.,0.,0.));
#9299=DIRECTION('',(0.,-1.,0.));
#9300=DIRECTION('center_axis',(0.,1.,0.));
#9301=DIRECTION('ref_axis',(1.,0.,0.));
#9302=DIRECTION('center_axis',(0.,1.,0.));
#9303=DIRECTION('ref_axis',(1.,0.,0.));
#9304=DIRECTION('center_axis',(0.,1.,0.));
#9305=DIRECTION('ref_axis',(0.,0.,1.));
#9306=DIRECTION('center_axis',(0.,-1.,0.));
#9307=DIRECTION('ref_axis',(1.,0.,0.));
#9308=DIRECTION('center_axis',(0.,-1.,0.));
#9309=DIRECTION('ref_axis',(1.,0.,0.));
#9310=DIRECTION('center_axis',(0.,-1.,0.));
#9311=DIRECTION('ref_axis',(1.,0.,0.));
#9312=DIRECTION('',(0.707106781186548,0.707106781186547,8.65956056235493E-17));
#9313=DIRECTION('center_axis',(0.,-1.,0.));
#9314=DIRECTION('ref_axis',(1.,0.,0.));
#9315=DIRECTION('center_axis',(0.,-1.,0.));
#9316=DIRECTION('ref_axis',(1.,0.,0.));
#9317=DIRECTION('',(0.,1.,0.));
#9318=DIRECTION('center_axis',(0.,1.,0.));
#9319=DIRECTION('ref_axis',(1.,0.,0.));
#9320=DIRECTION('center_axis',(0.,-1.,0.));
#9321=DIRECTION('ref_axis',(1.,0.,0.));
#9322=DIRECTION('',(-0.707106781186547,0.707106781186548,-8.65956056235493E-17));
#9323=DIRECTION('center_axis',(0.,-1.,0.));
#9324=DIRECTION('ref_axis',(0.,0.,-1.));
#9325=DIRECTION('center_axis',(0.,-1.,0.));
#9326=DIRECTION('ref_axis',(1.,0.,0.));
#9327=DIRECTION('center_axis',(0.,1.,0.));
#9328=DIRECTION('ref_axis',(1.,0.,0.));
#9329=DIRECTION('center_axis',(0.,1.,0.));
#9330=DIRECTION('ref_axis',(1.,0.,0.));
#9331=DIRECTION('',(-0.447213595499958,0.894427190999916,-5.47678698264203E-17));
#9332=DIRECTION('center_axis',(0.,-1.,0.));
#9333=DIRECTION('ref_axis',(1.,0.,0.));
#9334=DIRECTION('',(0.,1.,0.));
#13971=CARTESIAN_POINT('',(0.,0.,0.));
#13972=CARTESIAN_POINT('Origin',(0.115470053837925,-0.5,-0.2));
#13973=CARTESIAN_POINT('',(0.23094010767585,-0.5,0.));
#13974=CARTESIAN_POINT('',(0.115470053837925,-0.5,-0.2));
#13975=CARTESIAN_POINT('',(0.23094010767585,-0.5,0.));
#13976=CARTESIAN_POINT('',(0.115470053837925,-0.8,-0.2));
#13977=CARTESIAN_POINT('',(0.115470053837925,-0.5,-0.2));
#13978=CARTESIAN_POINT('',(0.23094010767585,-0.8,0.));
#13979=CARTESIAN_POINT('',(0.23094010767585,-0.8,0.));
#13980=CARTESIAN_POINT('',(0.23094010767585,-0.5,0.));
#13981=CARTESIAN_POINT('Origin',(-0.115470053837925,-0.5,-0.2));
#13982=CARTESIAN_POINT('',(-0.115470053837925,-0.5,-0.2));
#13983=CARTESIAN_POINT('',(0.115470053837925,-0.5,-0.2));
#13984=CARTESIAN_POINT('',(-0.115470053837925,-0.8,-0.2));
#13985=CARTESIAN_POINT('',(-0.115470053837925,-0.5,-0.2));
#13986=CARTESIAN_POINT('',(0.115470053837925,-0.8,-0.2));
#13987=CARTESIAN_POINT('Origin',(-0.23094010767585,-0.5,-2.77555756156289E-17));
#13988=CARTESIAN_POINT('',(-0.23094010767585,-0.5,-2.82820063659975E-17));
#13989=CARTESIAN_POINT('',(-0.115470053837925,-0.5,-0.2));
#13990=CARTESIAN_POINT('',(-0.23094010767585,-0.8,-2.77555756156289E-17));
#13991=CARTESIAN_POINT('',(-0.23094010767585,-0.5,-2.82820063659975E-17));
#13992=CARTESIAN_POINT('',(-0.115470053837925,-0.8,-0.2));
#13993=CARTESIAN_POINT('Origin',(-0.115470053837925,-0.5,0.2));
#13994=CARTESIAN_POINT('',(-0.115470053837925,-0.5,0.2));
#13995=CARTESIAN_POINT('',(-0.23094010767585,-0.5,-2.82820063659975E-17));
#13996=CARTESIAN_POINT('',(-0.115470053837925,-0.8,0.2));
#13997=CARTESIAN_POINT('',(-0.115470053837925,-0.5,0.2));
#13998=CARTESIAN_POINT('',(-0.23094010767585,-0.8,-2.82820063659975E-17));
#13999=CARTESIAN_POINT('Origin',(0.115470053837925,-0.5,0.2));
#14000=CARTESIAN_POINT('',(0.115470053837925,-0.5,0.2));
#14001=CARTESIAN_POINT('',(-0.115470053837925,-0.5,0.2));
#14002=CARTESIAN_POINT('',(0.115470053837925,-0.8,0.2));
#14003=CARTESIAN_POINT('',(0.115470053837925,-0.5,0.2));
#14004=CARTESIAN_POINT('',(-0.115470053837925,-0.8,0.2));
#14005=CARTESIAN_POINT('Origin',(0.23094010767585,-0.5,0.));
#14006=CARTESIAN_POINT('',(0.115470053837925,-0.5,0.2));
#14007=CARTESIAN_POINT('',(0.115470053837925,-0.8,0.2));
#14008=CARTESIAN_POINT('Origin',(0.,-0.5,0.));
#14009=CARTESIAN_POINT('Origin',(0.,-0.8,0.));
#14010=CARTESIAN_POINT('Origin',(0.,-1.9,0.));
#14011=CARTESIAN_POINT('',(-0.25,-1.9,3.06161699786838E-17));
#14012=CARTESIAN_POINT('Origin',(0.,-1.9,0.));
#14013=CARTESIAN_POINT('',(-0.24505,-1.9,3.00099698131059E-17));
#14014=CARTESIAN_POINT('Origin',(0.,-1.9,0.));
#14015=CARTESIAN_POINT('Origin',(0.,-3.,0.));
#14016=CARTESIAN_POINT('',(-0.25,-3.,3.06161699786838E-17));
#14017=CARTESIAN_POINT('',(-0.25,-3.,3.06161699786838E-17));
#14018=CARTESIAN_POINT('Origin',(0.,-3.,0.));
#14019=CARTESIAN_POINT('Origin',(0.,-3.,0.));
#14020=CARTESIAN_POINT('Origin',(0.375,0.5,0.));
#14021=CARTESIAN_POINT('',(-0.375,0.5,-4.59242549680257E-17));
#14022=CARTESIAN_POINT('Origin',(0.,0.5,0.));
#14023=CARTESIAN_POINT('Origin',(0.,0.475,0.));
#14024=CARTESIAN_POINT('',(-0.425,0.45,-5.20474889637625E-17));
#14025=CARTESIAN_POINT('Origin',(0.,0.45,0.));
#14026=CARTESIAN_POINT('',(-0.4,0.475,-4.89858719658941E-17));
#14027=CARTESIAN_POINT('Origin',(0.,0.24,0.));
#14028=CARTESIAN_POINT('',(-0.425,0.0299999999999998,-5.20474889637625E-17));
#14029=CARTESIAN_POINT('Origin',(0.,0.0299999999999998,0.));
#14030=CARTESIAN_POINT('',(-0.425,0.24,-5.20474889637625E-17));
#14031=CARTESIAN_POINT('Origin',(0.,0.0150000000000001,0.));
#14032=CARTESIAN_POINT('',(-0.395,4.85722573273506E-17,-4.83735485663204E-17));
#14033=CARTESIAN_POINT('Origin',(0.,0.,0.));
#14034=CARTESIAN_POINT('',(-0.41,0.0150000000000001,-5.02105187650415E-17));
#14035=CARTESIAN_POINT('Origin',(0.27,0.,0.));
#14036=CARTESIAN_POINT('',(-0.27,0.,-3.30654635769785E-17));
#14037=CARTESIAN_POINT('Origin',(0.,0.,0.));
#14038=CARTESIAN_POINT('Origin',(0.,-0.02,0.));
#14039=CARTESIAN_POINT('',(-0.24505,-0.0498999999999999,3.00099698131059E-17));
#14040=CARTESIAN_POINT('Origin',(0.,-0.0498999999999999,0.));
#14041=CARTESIAN_POINT('',(-0.26,-0.02,-3.18408167778312E-17));
#14042=CARTESIAN_POINT('Origin',(0.,-0.995,0.));
#14043=CARTESIAN_POINT('',(-0.24505,-0.995,-3.00099698131059E-17));
#14982=UNCERTAINTY_MEASURE_WITH_UNIT(LENGTH_MEASURE(0.001),#15041,
'DISTANCE_ACCURACY_VALUE',
'Maximum model space distance between geometric entities at asserted c
onnectivities');
#15000=UNCERTAINTY_MEASURE_WITH_UNIT(LENGTH_MEASURE(0.001),#15041,
'DISTANCE_ACCURACY_VALUE',
'Maximum model space distance between geometric entities at asserted c
onnectivities');
#15022=(
GEOMETRIC_REPRESENTATION_CONTEXT(3)
GLOBAL_UNCERTAINTY_ASSIGNED_CONTEXT((#14982))
GLOBAL_UNIT_ASSIGNED_CONTEXT((#15041,#15043,#15044))
REPRESENTATION_CONTEXT('','3D')
);
#15040=(
GEOMETRIC_REPRESENTATION_CONTEXT(3)
GLOBAL_UNCERTAINTY_ASSIGNED_CONTEXT((#15000))
GLOBAL_UNIT_ASSIGNED_CONTEXT((#15041,#15043,#15044))
REPRESENTATION_CONTEXT('','3D')
);
#15041=(
LENGTH_UNIT()
NAMED_UNIT(*)
SI_UNIT(.CENTI.,.METRE.)
);
#15043=(
NAMED_UNIT(*)
PLANE_ANGLE_UNIT()
SI_UNIT($,.RADIAN.)
);
#15044=(
NAMED_UNIT(*)
SI_UNIT($,.STERADIAN.)
SOLID_ANGLE_UNIT()
);
#15066=SHAPE_DEFINITION_REPRESENTATION(#15105,#15203);
#15105=PRODUCT_DEFINITION_SHAPE('',$,#15243);
#15203=SHAPE_REPRESENTATION('',(#7845),#15022);
#15221=PRODUCT_DEFINITION_CONTEXT('part definition',#15340,'design');
#15243=PRODUCT_DEFINITION('M5x30 frame screw','M5x30 frame screw',#15282,
#15221);
#15282=PRODUCT_DEFINITION_FORMATION('',$,#15363);
#15340=APPLICATION_CONTEXT(
'Core Data for Automotive Mechanical Design Process');
#15341=PRODUCT_CONTEXT('part definition',#15340,'mechanical');
#15363=PRODUCT('M5x30 frame screw','M5x30 frame screw',
'M5x30 frame screw',(#15341));
#15458=COLOUR_RGB('Black',0.12,0.14,0.17);
#15459=FILL_AREA_STYLE_COLOUR('',#15458);
#15460=FILL_AREA_STYLE('',(#15459));
#15461=SURFACE_STYLE_FILL_AREA(#15460);
#15462=SURFACE_SIDE_STYLE('',(#15461));
#15463=SURFACE_STYLE_USAGE(.BOTH.,#15462);
#15464=PRESENTATION_STYLE_ASSIGNMENT((#15463));
ENDSEC;
END-ISO-10303-21;
